ISO-10303-21;
HEADER;
/* Generated by software containing ST-Developer
 * from STEP Tools, Inc. (www.steptools.com) 
 */

FILE_DESCRIPTION(
/* description */ ('Flywheel Crank-Slider'),
/* implementation_level */ '2;1');

FILE_NAME(
/* name */ 'Bearing pedestal (1).step',
/* time_stamp */ '2026-10-28T03:23:13-07:00',
/* author */ (''),
/* organization */ (''),
/* preprocessor_version */ 'ST-DEVELOPER v20.2',
/* originating_system */ 'Autodesk Translation Framework v15.17.0.0',
/* authorisation */ '');

FILE_SCHEMA (('AUTOMOTIVE_DESIGN { 1 0 10303 214 3 1 1 }'));
ENDSEC;

DATA;
#10=MECHANICAL_DESIGN_GEOMETRIC_PRESENTATION_REPRESENTATION('',(#672),#17322);
#568=SHAPE_REPRESENTATION_RELATIONSHIP('SRR','None',#17564,#620);
#620=ADVANCED_BREP_SHAPE_REPRESENTATION('',(#733),#17268);
#672=STYLED_ITEM('',(#17931),#733);
#733=MANIFOLD_SOLID_BREP('Body1',#9050);
#827=FACE_BOUND('',#1951,.T.);
#828=FACE_BOUND('',#1954,.T.);
#829=FACE_BOUND('',#1957,.T.);
#830=FACE_BOUND('',#1960,.T.);
#831=FACE_BOUND('',#1970,.T.);
#832=FACE_BOUND('',#1971,.T.);
#833=FACE_BOUND('',#1972,.T.);
#834=FACE_BOUND('',#1973,.T.);
#835=FACE_BOUND('',#1974,.T.);
#836=FACE_BOUND('',#1975,.T.);
#837=FACE_BOUND('',#1977,.T.);
#838=FACE_BOUND('',#1978,.T.);
#839=FACE_BOUND('',#1979,.T.);
#840=FACE_BOUND('',#1980,.T.);
#1033=PLANE('',#9795);
#1034=PLANE('',#9799);
#1035=PLANE('',#9803);
#1036=PLANE('',#9808);
#1037=PLANE('',#9813);
#1038=PLANE('',#9818);
#1039=PLANE('',#9828);
#1040=PLANE('',#9829);
#1041=PLANE('',#9830);
#1042=PLANE('',#9831);
#1043=PLANE('',#9832);
#1044=PLANE('',#9833);
#1368=FACE_OUTER_BOUND('',#1945,.T.);
#1369=FACE_OUTER_BOUND('',#1946,.T.);
#1370=FACE_OUTER_BOUND('',#1947,.T.);
#1371=FACE_OUTER_BOUND('',#1948,.T.);
#1372=FACE_OUTER_BOUND('',#1949,.T.);
#1373=FACE_OUTER_BOUND('',#1950,.T.);
#1374=FACE_OUTER_BOUND('',#1952,.T.);
#1375=FACE_OUTER_BOUND('',#1953,.T.);
#1376=FACE_OUTER_BOUND('',#1955,.T.);
#1377=FACE_OUTER_BOUND('',#1956,.T.);
#1378=FACE_OUTER_BOUND('',#1958,.T.);
#1379=FACE_OUTER_BOUND('',#1959,.T.);
#1380=FACE_OUTER_BOUND('',#1961,.T.);
#1381=FACE_OUTER_BOUND('',#1962,.T.);
#1382=FACE_OUTER_BOUND('',#1963,.T.);
#1383=FACE_OUTER_BOUND('',#1964,.T.);
#1384=FACE_OUTER_BOUND('',#1965,.T.);
#1385=FACE_OUTER_BOUND('',#1966,.T.);
#1386=FACE_OUTER_BOUND('',#1967,.T.);
#1387=FACE_OUTER_BOUND('',#1968,.T.);
#1388=FACE_OUTER_BOUND('',#1969,.T.);
#1389=FACE_OUTER_BOUND('',#1976,.T.);
#1945=EDGE_LOOP('',(#6326,#6327,#6328,#6329));
#1946=EDGE_LOOP('',(#6330));
#1947=EDGE_LOOP('',(#6331,#6332,#6333,#6334));
#1948=EDGE_LOOP('',(#6335));
#1949=EDGE_LOOP('',(#6336,#6337,#6338,#6339));
#1950=EDGE_LOOP('',(#6340));
#1951=EDGE_LOOP('',(#6341));
#1952=EDGE_LOOP('',(#6342,#6343,#6344,#6345));
#1953=EDGE_LOOP('',(#6346));
#1954=EDGE_LOOP('',(#6347));
#1955=EDGE_LOOP('',(#6348,#6349,#6350,#6351));
#1956=EDGE_LOOP('',(#6352));
#1957=EDGE_LOOP('',(#6353));
#1958=EDGE_LOOP('',(#6354,#6355,#6356,#6357));
#1959=EDGE_LOOP('',(#6358));
#1960=EDGE_LOOP('',(#6359));
#1961=EDGE_LOOP('',(#6360,#6361,#6362,#6363));
#1962=EDGE_LOOP('',(#6364,#6365,#6366,#6367));
#1963=EDGE_LOOP('',(#6368,#6369,#6370,#6371));
#1964=EDGE_LOOP('',(#6372,#6373,#6374,#6375));
#1965=EDGE_LOOP('',(#6376,#6377,#6378,#6379));
#1966=EDGE_LOOP('',(#6380,#6381,#6382,#6383));
#1967=EDGE_LOOP('',(#6384,#6385,#6386,#6387));
#1968=EDGE_LOOP('',(#6388,#6389,#6390,#6391));
#1969=EDGE_LOOP('',(#6392,#6393,#6394,#6395));
#1970=EDGE_LOOP('',(#6396));
#1971=EDGE_LOOP('',(#6397));
#1972=EDGE_LOOP('',(#6398));
#1973=EDGE_LOOP('',(#6399));
#1974=EDGE_LOOP('',(#6400));
#1975=EDGE_LOOP('',(#6401));
#1976=EDGE_LOOP('',(#6402,#6403,#6404,#6405));
#1977=EDGE_LOOP('',(#6406));
#1978=EDGE_LOOP('',(#6407));
#1979=EDGE_LOOP('',(#6408));
#1980=EDGE_LOOP('',(#6409));
#2666=LINE('',#13960,#3277);
#2667=LINE('',#13967,#3278);
#2668=LINE('',#13974,#3279);
#2669=LINE('',#13983,#3280);
#2670=LINE('',#13992,#3281);
#2671=LINE('',#14001,#3282);
#2672=LINE('',#14009,#3283);
#2673=LINE('',#14013,#3284);
#2674=LINE('',#14017,#3285);
#2675=LINE('',#14021,#3286);
#2676=LINE('',#14025,#3287);
#2677=LINE('',#14027,#3288);
#2678=LINE('',#14029,#3289);
#2679=LINE('',#14030,#3290);
#2680=LINE('',#14033,#3291);
#2681=LINE('',#14035,#3292);
#2682=LINE('',#14036,#3293);
#2683=LINE('',#14039,#3294);
#2684=LINE('',#14041,#3295);
#2685=LINE('',#14042,#3296);
#2686=LINE('',#14044,#3297);
#2687=LINE('',#14045,#3298);
#3277=VECTOR('',#11098,0.34);
#3278=VECTOR('',#11107,0.34);
#3279=VECTOR('',#11116,0.5);
#3280=VECTOR('',#11127,0.5);
#3281=VECTOR('',#11138,0.5);
#3282=VECTOR('',#11149,0.5);
#3283=VECTOR('',#11160,0.275);
#3284=VECTOR('',#11165,0.275);
#3285=VECTOR('',#11170,0.275);
#3286=VECTOR('',#11175,0.275);
#3287=VECTOR('',#11178,1.);
#3288=VECTOR('',#11179,1.);
#3289=VECTOR('',#11180,1.);
#3290=VECTOR('',#11181,1.);
#3291=VECTOR('',#11184,1.);
#3292=VECTOR('',#11185,1.);
#3293=VECTOR('',#11186,1.);
#3294=VECTOR('',#11189,1.);
#3295=VECTOR('',#11190,1.);
#3296=VECTOR('',#11191,1.);
#3297=VECTOR('',#11194,1.);
#3298=VECTOR('',#11195,1.);
#3890=CIRCLE('',#9793,0.34);
#3891=CIRCLE('',#9794,0.34);
#3892=CIRCLE('',#9797,0.34);
#3893=CIRCLE('',#9798,0.34);
#3894=CIRCLE('',#9801,0.5);
#3895=CIRCLE('',#9802,0.5);
#3896=CIRCLE('',#9804,0.275);
#3897=CIRCLE('',#9806,0.5);
#3898=CIRCLE('',#9807,0.5);
#3899=CIRCLE('',#9809,0.275);
#3900=CIRCLE('',#9811,0.5);
#3901=CIRCLE('',#9812,0.5);
#3902=CIRCLE('',#9814,0.275);
#3903=CIRCLE('',#9816,0.5);
#3904=CIRCLE('',#9817,0.5);
#3905=CIRCLE('',#9819,0.275);
#3906=CIRCLE('',#9821,0.275);
#3907=CIRCLE('',#9823,0.275);
#3908=CIRCLE('',#9825,0.275);
#3909=CIRCLE('',#9827,0.275);
#4345=VERTEX_POINT('',#13957);
#4346=VERTEX_POINT('',#13959);
#4347=VERTEX_POINT('',#13964);
#4348=VERTEX_POINT('',#13966);
#4349=VERTEX_POINT('',#13971);
#4350=VERTEX_POINT('',#13973);
#4351=VERTEX_POINT('',#13977);
#4352=VERTEX_POINT('',#13980);
#4353=VERTEX_POINT('',#13982);
#4354=VERTEX_POINT('',#13986);
#4355=VERTEX_POINT('',#13989);
#4356=VERTEX_POINT('',#13991);
#4357=VERTEX_POINT('',#13995);
#4358=VERTEX_POINT('',#13998);
#4359=VERTEX_POINT('',#14000);
#4360=VERTEX_POINT('',#14004);
#4361=VERTEX_POINT('',#14007);
#4362=VERTEX_POINT('',#14011);
#4363=VERTEX_POINT('',#14015);
#4364=VERTEX_POINT('',#14019);
#4365=VERTEX_POINT('',#14023);
#4366=VERTEX_POINT('',#14024);
#4367=VERTEX_POINT('',#14026);
#4368=VERTEX_POINT('',#14028);
#4369=VERTEX_POINT('',#14032);
#4370=VERTEX_POINT('',#14034);
#4371=VERTEX_POINT('',#14038);
#4372=VERTEX_POINT('',#14040);
#5120=EDGE_CURVE('',#4345,#4345,#3890,.T.);
#5121=EDGE_CURVE('',#4345,#4346,#2666,.T.);
#5122=EDGE_CURVE('',#4346,#4346,#3891,.T.);
#5123=EDGE_CURVE('',#4347,#4347,#3892,.T.);
#5124=EDGE_CURVE('',#4347,#4348,#2667,.T.);
#5125=EDGE_CURVE('',#4348,#4348,#3893,.T.);
#5126=EDGE_CURVE('',#4349,#4349,#3894,.T.);
#5127=EDGE_CURVE('',#4349,#4350,#2668,.T.);
#5128=EDGE_CURVE('',#4350,#4350,#3895,.T.);
#5129=EDGE_CURVE('',#4351,#4351,#3896,.T.);
#5130=EDGE_CURVE('',#4352,#4352,#3897,.T.);
#5131=EDGE_CURVE('',#4352,#4353,#2669,.T.);
#5132=EDGE_CURVE('',#4353,#4353,#3898,.T.);
#5133=EDGE_CURVE('',#4354,#4354,#3899,.T.);
#5134=EDGE_CURVE('',#4355,#4355,#3900,.T.);
#5135=EDGE_CURVE('',#4355,#4356,#2670,.T.);
#5136=EDGE_CURVE('',#4356,#4356,#3901,.T.);
#5137=EDGE_CURVE('',#4357,#4357,#3902,.T.);
#5138=EDGE_CURVE('',#4358,#4358,#3903,.T.);
#5139=EDGE_CURVE('',#4358,#4359,#2671,.T.);
#5140=EDGE_CURVE('',#4359,#4359,#3904,.T.);
#5141=EDGE_CURVE('',#4360,#4360,#3905,.T.);
#5142=EDGE_CURVE('',#4361,#4361,#3906,.T.);
#5143=EDGE_CURVE('',#4361,#4351,#2672,.T.);
#5144=EDGE_CURVE('',#4362,#4362,#3907,.T.);
#5145=EDGE_CURVE('',#4362,#4354,#2673,.T.);
#5146=EDGE_CURVE('',#4363,#4363,#3908,.T.);
#5147=EDGE_CURVE('',#4363,#4357,#2674,.T.);
#5148=EDGE_CURVE('',#4364,#4364,#3909,.T.);
#5149=EDGE_CURVE('',#4364,#4360,#2675,.T.);
#5150=EDGE_CURVE('',#4365,#4366,#2676,.T.);
#5151=EDGE_CURVE('',#4366,#4367,#2677,.T.);
#5152=EDGE_CURVE('',#4368,#4367,#2678,.T.);
#5153=EDGE_CURVE('',#4365,#4368,#2679,.T.);
#5154=EDGE_CURVE('',#4369,#4365,#2680,.T.);
#5155=EDGE_CURVE('',#4370,#4368,#2681,.T.);
#5156=EDGE_CURVE('',#4369,#4370,#2682,.T.);
#5157=EDGE_CURVE('',#4371,#4369,#2683,.T.);
#5158=EDGE_CURVE('',#4372,#4370,#2684,.T.);
#5159=EDGE_CURVE('',#4371,#4372,#2685,.T.);
#5160=EDGE_CURVE('',#4366,#4371,#2686,.T.);
#5161=EDGE_CURVE('',#4367,#4372,#2687,.T.);
#6326=ORIENTED_EDGE('',*,*,#5120,.F.);
#6327=ORIENTED_EDGE('',*,*,#5121,.T.);
#6328=ORIENTED_EDGE('',*,*,#5122,.F.);
#6329=ORIENTED_EDGE('',*,*,#5121,.F.);
#6330=ORIENTED_EDGE('',*,*,#5120,.T.);
#6331=ORIENTED_EDGE('',*,*,#5123,.F.);
#6332=ORIENTED_EDGE('',*,*,#5124,.T.);
#6333=ORIENTED_EDGE('',*,*,#5125,.F.);
#6334=ORIENTED_EDGE('',*,*,#5124,.F.);
#6335=ORIENTED_EDGE('',*,*,#5123,.T.);
#6336=ORIENTED_EDGE('',*,*,#5126,.F.);
#6337=ORIENTED_EDGE('',*,*,#5127,.T.);
#6338=ORIENTED_EDGE('',*,*,#5128,.F.);
#6339=ORIENTED_EDGE('',*,*,#5127,.F.);
#6340=ORIENTED_EDGE('',*,*,#5126,.T.);
#6341=ORIENTED_EDGE('',*,*,#5129,.F.);
#6342=ORIENTED_EDGE('',*,*,#5130,.F.);
#6343=ORIENTED_EDGE('',*,*,#5131,.T.);
#6344=ORIENTED_EDGE('',*,*,#5132,.F.);
#6345=ORIENTED_EDGE('',*,*,#5131,.F.);
#6346=ORIENTED_EDGE('',*,*,#5130,.T.);
#6347=ORIENTED_EDGE('',*,*,#5133,.F.);
#6348=ORIENTED_EDGE('',*,*,#5134,.F.);
#6349=ORIENTED_EDGE('',*,*,#5135,.T.);
#6350=ORIENTED_EDGE('',*,*,#5136,.F.);
#6351=ORIENTED_EDGE('',*,*,#5135,.F.);
#6352=ORIENTED_EDGE('',*,*,#5134,.T.);
#6353=ORIENTED_EDGE('',*,*,#5137,.F.);
#6354=ORIENTED_EDGE('',*,*,#5138,.F.);
#6355=ORIENTED_EDGE('',*,*,#5139,.T.);
#6356=ORIENTED_EDGE('',*,*,#5140,.F.);
#6357=ORIENTED_EDGE('',*,*,#5139,.F.);
#6358=ORIENTED_EDGE('',*,*,#5138,.T.);
#6359=ORIENTED_EDGE('',*,*,#5141,.F.);
#6360=ORIENTED_EDGE('',*,*,#5142,.F.);
#6361=ORIENTED_EDGE('',*,*,#5143,.T.);
#6362=ORIENTED_EDGE('',*,*,#5129,.T.);
#6363=ORIENTED_EDGE('',*,*,#5143,.F.);
#6364=ORIENTED_EDGE('',*,*,#5144,.F.);
#6365=ORIENTED_EDGE('',*,*,#5145,.T.);
#6366=ORIENTED_EDGE('',*,*,#5133,.T.);
#6367=ORIENTED_EDGE('',*,*,#5145,.F.);
#6368=ORIENTED_EDGE('',*,*,#5146,.F.);
#6369=ORIENTED_EDGE('',*,*,#5147,.T.);
#6370=ORIENTED_EDGE('',*,*,#5137,.T.);
#6371=ORIENTED_EDGE('',*,*,#5147,.F.);
#6372=ORIENTED_EDGE('',*,*,#5148,.F.);
#6373=ORIENTED_EDGE('',*,*,#5149,.T.);
#6374=ORIENTED_EDGE('',*,*,#5141,.T.);
#6375=ORIENTED_EDGE('',*,*,#5149,.F.);
#6376=ORIENTED_EDGE('',*,*,#5150,.T.);
#6377=ORIENTED_EDGE('',*,*,#5151,.T.);
#6378=ORIENTED_EDGE('',*,*,#5152,.F.);
#6379=ORIENTED_EDGE('',*,*,#5153,.F.);
#6380=ORIENTED_EDGE('',*,*,#5154,.T.);
#6381=ORIENTED_EDGE('',*,*,#5153,.T.);
#6382=ORIENTED_EDGE('',*,*,#5155,.F.);
#6383=ORIENTED_EDGE('',*,*,#5156,.F.);
#6384=ORIENTED_EDGE('',*,*,#5157,.T.);
#6385=ORIENTED_EDGE('',*,*,#5156,.T.);
#6386=ORIENTED_EDGE('',*,*,#5158,.F.);
#6387=ORIENTED_EDGE('',*,*,#5159,.F.);
#6388=ORIENTED_EDGE('',*,*,#5160,.T.);
#6389=ORIENTED_EDGE('',*,*,#5159,.T.);
#6390=ORIENTED_EDGE('',*,*,#5161,.F.);
#6391=ORIENTED_EDGE('',*,*,#5151,.F.);
#6392=ORIENTED_EDGE('',*,*,#5161,.T.);
#6393=ORIENTED_EDGE('',*,*,#5158,.T.);
#6394=ORIENTED_EDGE('',*,*,#5155,.T.);
#6395=ORIENTED_EDGE('',*,*,#5152,.T.);
#6396=ORIENTED_EDGE('',*,*,#5122,.T.);
#6397=ORIENTED_EDGE('',*,*,#5125,.T.);
#6398=ORIENTED_EDGE('',*,*,#5140,.T.);
#6399=ORIENTED_EDGE('',*,*,#5136,.T.);
#6400=ORIENTED_EDGE('',*,*,#5132,.T.);
#6401=ORIENTED_EDGE('',*,*,#5128,.T.);
#6402=ORIENTED_EDGE('',*,*,#5160,.F.);
#6403=ORIENTED_EDGE('',*,*,#5150,.F.);
#6404=ORIENTED_EDGE('',*,*,#5154,.F.);
#6405=ORIENTED_EDGE('',*,*,#5157,.F.);
#6406=ORIENTED_EDGE('',*,*,#5142,.T.);
#6407=ORIENTED_EDGE('',*,*,#5144,.T.);
#6408=ORIENTED_EDGE('',*,*,#5146,.T.);
#6409=ORIENTED_EDGE('',*,*,#5148,.T.);
#8356=CYLINDRICAL_SURFACE('',#9792,0.34);
#8357=CYLINDRICAL_SURFACE('',#9796,0.34);
#8358=CYLINDRICAL_SURFACE('',#9800,0.5);
#8359=CYLINDRICAL_SURFACE('',#9805,0.5);
#8360=CYLINDRICAL_SURFACE('',#9810,0.5);
#8361=CYLINDRICAL_SURFACE('',#9815,0.5);
#8362=CYLINDRICAL_SURFACE('',#9820,0.275);
#8363=CYLINDRICAL_SURFACE('',#9822,0.275);
#8364=CYLINDRICAL_SURFACE('',#9824,0.275);
#8365=CYLINDRICAL_SURFACE('',#9826,0.275);
#8559=ADVANCED_FACE('',(#1368),#8356,.F.);
#8560=ADVANCED_FACE('',(#1369),#1033,.T.);
#8561=ADVANCED_FACE('',(#1370),#8357,.F.);
#8562=ADVANCED_FACE('',(#1371),#1034,.T.);
#8563=ADVANCED_FACE('',(#1372),#8358,.F.);
#8564=ADVANCED_FACE('',(#1373,#827),#1035,.T.);
#8565=ADVANCED_FACE('',(#1374),#8359,.F.);
#8566=ADVANCED_FACE('',(#1375,#828),#1036,.T.);
#8567=ADVANCED_FACE('',(#1376),#8360,.F.);
#8568=ADVANCED_FACE('',(#1377,#829),#1037,.T.);
#8569=ADVANCED_FACE('',(#1378),#8361,.F.);
#8570=ADVANCED_FACE('',(#1379,#830),#1038,.T.);
#8571=ADVANCED_FACE('',(#1380),#8362,.F.);
#8572=ADVANCED_FACE('',(#1381),#8363,.F.);
#8573=ADVANCED_FACE('',(#1382),#8364,.F.);
#8574=ADVANCED_FACE('',(#1383),#8365,.F.);
#8575=ADVANCED_FACE('',(#1384),#1039,.T.);
#8576=ADVANCED_FACE('',(#1385),#1040,.T.);
#8577=ADVANCED_FACE('',(#1386),#1041,.T.);
#8578=ADVANCED_FACE('',(#1387),#1042,.T.);
#8579=ADVANCED_FACE('',(#1388,#831,#832,#833,#834,#835,#836),#1043,.T.);
#8580=ADVANCED_FACE('',(#1389,#837,#838,#839,#840),#1044,.F.);
#9050=CLOSED_SHELL('',(#8559,#8560,#8561,#8562,#8563,#8564,#8565,#8566,
#8567,#8568,#8569,#8570,#8571,#8572,#8573,#8574,#8575,#8576,#8577,#8578,
#8579,#8580));
#9791=AXIS2_PLACEMENT_3D('',#13955,#11092,#11093);
#9792=AXIS2_PLACEMENT_3D('',#13956,#11094,#11095);
#9793=AXIS2_PLACEMENT_3D('',#13958,#11096,#11097);
#9794=AXIS2_PLACEMENT_3D('',#13961,#11099,#11100);
#9795=AXIS2_PLACEMENT_3D('',#13962,#11101,#11102);
#9796=AXIS2_PLACEMENT_3D('',#13963,#11103,#11104);
#9797=AXIS2_PLACEMENT_3D('',#13965,#11105,#11106);
#9798=AXIS2_PLACEMENT_3D('',#13968,#11108,#11109);
#9799=AXIS2_PLACEMENT_3D('',#13969,#11110,#11111);
#9800=AXIS2_PLACEMENT_3D('',#13970,#11112,#11113);
#9801=AXIS2_PLACEMENT_3D('',#13972,#11114,#11115);
#9802=AXIS2_PLACEMENT_3D('',#13975,#11117,#11118);
#9803=AXIS2_PLACEMENT_3D('',#13976,#11119,#11120);
#9804=AXIS2_PLACEMENT_3D('',#13978,#11121,#11122);
#9805=AXIS2_PLACEMENT_3D('',#13979,#11123,#11124);
#9806=AXIS2_PLACEMENT_3D('',#13981,#11125,#11126);
#9807=AXIS2_PLACEMENT_3D('',#13984,#11128,#11129);
#9808=AXIS2_PLACEMENT_3D('',#13985,#11130,#11131);
#9809=AXIS2_PLACEMENT_3D('',#13987,#11132,#11133);
#9810=AXIS2_PLACEMENT_3D('',#13988,#11134,#11135);
#9811=AXIS2_PLACEMENT_3D('',#13990,#11136,#11137);
#9812=AXIS2_PLACEMENT_3D('',#13993,#11139,#11140);
#9813=AXIS2_PLACEMENT_3D('',#13994,#11141,#11142);
#9814=AXIS2_PLACEMENT_3D('',#13996,#11143,#11144);
#9815=AXIS2_PLACEMENT_3D('',#13997,#11145,#11146);
#9816=AXIS2_PLACEMENT_3D('',#13999,#11147,#11148);
#9817=AXIS2_PLACEMENT_3D('',#14002,#11150,#11151);
#9818=AXIS2_PLACEMENT_3D('',#14003,#11152,#11153);
#9819=AXIS2_PLACEMENT_3D('',#14005,#11154,#11155);
#9820=AXIS2_PLACEMENT_3D('',#14006,#11156,#11157);
#9821=AXIS2_PLACEMENT_3D('',#14008,#11158,#11159);
#9822=AXIS2_PLACEMENT_3D('',#14010,#11161,#11162);
#9823=AXIS2_PLACEMENT_3D('',#14012,#11163,#11164);
#9824=AXIS2_PLACEMENT_3D('',#14014,#11166,#11167);
#9825=AXIS2_PLACEMENT_3D('',#14016,#11168,#11169);
#9826=AXIS2_PLACEMENT_3D('',#14018,#11171,#11172);
#9827=AXIS2_PLACEMENT_3D('',#14020,#11173,#11174);
#9828=AXIS2_PLACEMENT_3D('',#14022,#11176,#11177);
#9829=AXIS2_PLACEMENT_3D('',#14031,#11182,#11183);
#9830=AXIS2_PLACEMENT_3D('',#14037,#11187,#11188);
#9831=AXIS2_PLACEMENT_3D('',#14043,#11192,#11193);
#9832=AXIS2_PLACEMENT_3D('',#14046,#11196,#11197);
#9833=AXIS2_PLACEMENT_3D('',#14047,#11198,#11199);
#11092=DIRECTION('axis',(0.,0.,1.));
#11093=DIRECTION('refdir',(1.,0.,0.));
#11094=DIRECTION('center_axis',(0.,0.,1.));
#11095=DIRECTION('ref_axis',(1.,0.,0.));
#11096=DIRECTION('center_axis',(0.,0.,1.));
#11097=DIRECTION('ref_axis',(1.,0.,0.));
#11098=DIRECTION('',(0.,0.,1.));
#11099=DIRECTION('center_axis',(0.,0.,-1.));
#11100=DIRECTION('ref_axis',(1.,0.,0.));
#11101=DIRECTION('center_axis',(0.,0.,1.));
#11102=DIRECTION('ref_axis',(1.,0.,0.));
#11103=DIRECTION('center_axis',(0.,0.,1.));
#11104=DIRECTION('ref_axis',(1.,0.,0.));
#11105=DIRECTION('center_axis',(0.,0.,1.));
#11106=DIRECTION('ref_axis',(1.,0.,0.));
#11107=DIRECTION('',(0.,0.,1.));
#11108=DIRECTION('center_axis',(0.,0.,-1.));
#11109=DIRECTION('ref_axis',(1.,0.,0.));
#11110=DIRECTION('center_axis',(0.,0.,1.));
#11111=DIRECTION('ref_axis',(1.,0.,0.));
#11112=DIRECTION('center_axis',(0.,0.,1.));
#11113=DIRECTION('ref_axis',(1.,0.,0.));
#11114=DIRECTION('center_axis',(0.,0.,1.));
#11115=DIRECTION('ref_axis',(1.,0.,0.));
#11116=DIRECTION('',(0.,0.,1.));
#11117=DIRECTION('center_axis',(0.,0.,-1.));
#11118=DIRECTION('ref_axis',(1.,0.,0.));
#11119=DIRECTION('center_axis',(0.,0.,1.));
#11120=DIRECTION('ref_axis',(1.,0.,0.));
#11121=DIRECTION('center_axis',(0.,0.,1.));
#11122=DIRECTION('ref_axis',(1.,0.,0.));
#11123=DIRECTION('center_axis',(0.,0.,1.));
#11124=DIRECTION('ref_axis',(1.,0.,0.));
#11125=DIRECTION('center_axis',(0.,0.,1.));
#11126=DIRECTION('ref_axis',(1.,0.,0.));
#11127=DIRECTION('',(0.,0.,1.));
#11128=DIRECTION('center_axis',(0.,0.,-1.));
#11129=DIRECTION('ref_axis',(1.,0.,0.));
#11130=DIRECTION('center_axis',(0.,0.,1.));
#11131=DIRECTION('ref_axis',(1.,0.,0.));
#11132=DIRECTION('center_axis',(0.,0.,1.));
#11133=DIRECTION('ref_axis',(1.,0.,0.));
#11134=DIRECTION('center_axis',(0.,0.,1.));
#11135=DIRECTION('ref_axis',(1.,0.,0.));
#11136=DIRECTION('center_axis',(0.,0.,1.));
#11137=DIRECTION('ref_axis',(1.,0.,0.));
#11138=DIRECTION('',(0.,0.,1.));
#11139=DIRECTION('center_axis',(0.,0.,-1.));
#11140=DIRECTION('ref_axis',(1.,0.,0.));
#11141=DIRECTION('center_axis',(0.,0.,1.));
#11142=DIRECTION('ref_axis',(1.,0.,0.));
#11143=DIRECTION('center_axis',(0.,0.,1.));
#11144=DIRECTION('ref_axis',(1.,0.,0.));
#11145=DIRECTION('center_axis',(0.,0.,1.));
#11146=DIRECTION('ref_axis',(1.,0.,0.));
#11147=DIRECTION('center_axis',(0.,0.,1.));
#11148=DIRECTION('ref_axis',(1.,0.,0.));
#11149=DIRECTION('',(0.,0.,1.));
#11150=DIRECTION('center_axis',(0.,0.,-1.));
#11151=DIRECTION('ref_axis',(1.,0.,0.));
#11152=DIRECTION('center_axis',(0.,0.,1.));
#11153=DIRECTION('ref_axis',(1.,0.,0.));
#11154=DIRECTION('center_axis',(0.,0.,1.));
#11155=DIRECTION('ref_axis',(1.,0.,0.));
#11156=DIRECTION('center_axis',(0.,0.,1.));
#11157=DIRECTION('ref_axis',(1.,0.,0.));
#11158=DIRECTION('center_axis',(0.,0.,1.));
#11159=DIRECTION('ref_axis',(1.,0.,0.));
#11160=DIRECTION('',(0.,0.,1.));
#11161=DIRECTION('center_axis',(0.,0.,1.));
#11162=DIRECTION('ref_axis',(1.,0.,0.));
#11163=DIRECTION('center_axis',(0.,0.,1.));
#11164=DIRECTION('ref_axis',(1.,0.,0.));
#11165=DIRECTION('',(0.,0.,1.));
#11166=DIRECTION('center_axis',(0.,0.,1.));
#11167=DIRECTION('ref_axis',(1.,0.,0.));
#11168=DIRECTION('center_axis',(0.,0.,1.));
#11169=DIRECTION('ref_axis',(1.,0.,0.));
#11170=DIRECTION('',(0.,0.,1.));
#11171=DIRECTION('center_axis',(0.,0.,1.));
#11172=DIRECTION('ref_axis',(1.,0.,0.));
#11173=DIRECTION('center_axis',(0.,0.,1.));
#11174=DIRECTION('ref_axis',(1.,0.,0.));
#11175=DIRECTION('',(0.,0.,1.));
#11176=DIRECTION('center_axis',(0.,1.,0.));
#11177=DIRECTION('ref_axis',(-1.,0.,0.));
#11178=DIRECTION('',(-1.,0.,0.));
#11179=DIRECTION('',(0.,0.,1.));
#11180=DIRECTION('',(-1.,0.,0.));
#11181=DIRECTION('',(0.,0.,1.));
#11182=DIRECTION('center_axis',(1.,0.,0.));
#11183=DIRECTION('ref_axis',(0.,1.,0.));
#11184=DIRECTION('',(0.,1.,0.));
#11185=DIRECTION('',(0.,1.,0.));
#11186=DIRECTION('',(0.,0.,1.));
#11187=DIRECTION('center_axis',(0.,-1.,0.));
#11188=DIRECTION('ref_axis',(1.,0.,0.));
#11189=DIRECTION('',(1.,0.,0.));
#11190=DIRECTION('',(1.,0.,0.));
#11191=DIRECTION('',(0.,0.,1.));
#11192=DIRECTION('center_axis',(-1.,0.,0.));
#11193=DIRECTION('ref_axis',(0.,-1.,0.));
#11194=DIRECTION('',(0.,-1.,0.));
#11195=DIRECTION('',(0.,-1.,0.));
#11196=DIRECTION('center_axis',(0.,0.,1.));
#11197=DIRECTION('ref_axis',(1.,0.,0.));
#11198=DIRECTION('center_axis',(0.,0.,1.));
#11199=DIRECTION('ref_axis',(1.,0.,0.));
#13955=CARTESIAN_POINT('',(0.,0.,0.));
#13956=CARTESIAN_POINT('Origin',(-4.75,-7.,5.3));
#13957=CARTESIAN_POINT('',(-5.09,-7.,5.3));
#13958=CARTESIAN_POINT('Origin',(-4.75,-7.,5.3));
#13959=CARTESIAN_POINT('',(-5.09,-7.,6.67));
#13960=CARTESIAN_POINT('',(-5.09,-7.,5.3));
#13961=CARTESIAN_POINT('Origin',(-4.75,-7.,6.67));
#13962=CARTESIAN_POINT('Origin',(-4.75,-7.,5.3));
#13963=CARTESIAN_POINT('Origin',(4.75,-7.,5.3));
#13964=CARTESIAN_POINT('',(4.41,-7.,5.3));
#13965=CARTESIAN_POINT('Origin',(4.75,-7.,5.3));
#13966=CARTESIAN_POINT('',(4.41,-7.,6.67));
#13967=CARTESIAN_POINT('',(4.41,-7.,5.3));
#13968=CARTESIAN_POINT('Origin',(4.75,-7.,6.67));
#13969=CARTESIAN_POINT('Origin',(4.75,-7.,5.3));
#13970=CARTESIAN_POINT('Origin',(5.8,-8.5,2.2));
#13971=CARTESIAN_POINT('',(5.3,-8.5,2.2));
#13972=CARTESIAN_POINT('Origin',(5.8,-8.5,2.2));
#13973=CARTESIAN_POINT('',(5.3,-8.5,6.67));
#13974=CARTESIAN_POINT('',(5.3,-8.5,2.2));
#13975=CARTESIAN_POINT('Origin',(5.8,-8.5,6.67));
#13976=CARTESIAN_POINT('Origin',(5.8,-8.5,2.2));
#13977=CARTESIAN_POINT('',(5.525,-8.5,2.2));
#13978=CARTESIAN_POINT('Origin',(5.8,-8.5,2.2));
#13979=CARTESIAN_POINT('Origin',(-5.8,-5.5,2.2));
#13980=CARTESIAN_POINT('',(-6.3,-5.5,2.2));
#13981=CARTESIAN_POINT('Origin',(-5.8,-5.5,2.2));
#13982=CARTESIAN_POINT('',(-6.3,-5.5,6.67));
#13983=CARTESIAN_POINT('',(-6.3,-5.5,2.2));
#13984=CARTESIAN_POINT('Origin',(-5.8,-5.5,6.67));
#13985=CARTESIAN_POINT('Origin',(-5.8,-5.5,2.2));
#13986=CARTESIAN_POINT('',(-6.075,-5.5,2.2));
#13987=CARTESIAN_POINT('Origin',(-5.8,-5.5,2.2));
#13988=CARTESIAN_POINT('Origin',(-5.8,-8.5,2.2));
#13989=CARTESIAN_POINT('',(-6.3,-8.5,2.2));
#13990=CARTESIAN_POINT('Origin',(-5.8,-8.5,2.2));
#13991=CARTESIAN_POINT('',(-6.3,-8.5,6.67));
#13992=CARTESIAN_POINT('',(-6.3,-8.5,2.2));
#13993=CARTESIAN_POINT('Origin',(-5.8,-8.5,6.67));
#13994=CARTESIAN_POINT('Origin',(-5.8,-8.5,2.2));
#13995=CARTESIAN_POINT('',(-6.075,-8.5,2.2));
#13996=CARTESIAN_POINT('Origin',(-5.8,-8.5,2.2));
#13997=CARTESIAN_POINT('Origin',(5.8,-5.5,2.2));
#13998=CARTESIAN_POINT('',(5.3,-5.5,2.2));
#13999=CARTESIAN_POINT('Origin',(5.8,-5.5,2.2));
#14000=CARTESIAN_POINT('',(5.3,-5.5,6.67));
#14001=CARTESIAN_POINT('',(5.3,-5.5,2.2));
#14002=CARTESIAN_POINT('Origin',(5.8,-5.5,6.67));
#14003=CARTESIAN_POINT('Origin',(5.8,-5.5,2.2));
#14004=CARTESIAN_POINT('',(5.525,-5.5,2.2));
#14005=CARTESIAN_POINT('Origin',(5.8,-5.5,2.2));
#14006=CARTESIAN_POINT('Origin',(5.8,-8.5,0.9));
#14007=CARTESIAN_POINT('',(5.525,-8.5,1.));
#14008=CARTESIAN_POINT('Origin',(5.8,-8.5,1.));
#14009=CARTESIAN_POINT('',(5.525,-8.5,0.9));
#14010=CARTESIAN_POINT('Origin',(-5.8,-5.5,0.9));
#14011=CARTESIAN_POINT('',(-6.075,-5.5,1.));
#14012=CARTESIAN_POINT('Origin',(-5.8,-5.5,1.));
#14013=CARTESIAN_POINT('',(-6.075,-5.5,0.9));
#14014=CARTESIAN_POINT('Origin',(-5.8,-8.5,0.9));
#14015=CARTESIAN_POINT('',(-6.075,-8.5,1.));
#14016=CARTESIAN_POINT('Origin',(-5.8,-8.5,1.));
#14017=CARTESIAN_POINT('',(-6.075,-8.5,0.9));
#14018=CARTESIAN_POINT('Origin',(5.8,-5.5,0.9));
#14019=CARTESIAN_POINT('',(5.525,-5.5,1.));
#14020=CARTESIAN_POINT('Origin',(5.8,-5.5,1.));
#14021=CARTESIAN_POINT('',(5.525,-5.5,0.9));
#14022=CARTESIAN_POINT('Origin',(7.,-4.75,1.));
#14023=CARTESIAN_POINT('',(7.,-4.75,1.));
#14024=CARTESIAN_POINT('',(-7.,-4.75,1.));
#14025=CARTESIAN_POINT('',(7.,-4.75,1.));
#14026=CARTESIAN_POINT('',(-7.,-4.75,6.67));
#14027=CARTESIAN_POINT('',(-7.,-4.75,1.));
#14028=CARTESIAN_POINT('',(7.,-4.75,6.67));
#14029=CARTESIAN_POINT('',(7.,-4.75,6.67));
#14030=CARTESIAN_POINT('',(7.,-4.75,1.));
#14031=CARTESIAN_POINT('Origin',(7.,-9.25,1.));
#14032=CARTESIAN_POINT('',(7.,-9.25,1.));
#14033=CARTESIAN_POINT('',(7.,-9.25,1.));
#14034=CARTESIAN_POINT('',(7.,-9.25,6.67));
#14035=CARTESIAN_POINT('',(7.,-9.25,6.67));
#14036=CARTESIAN_POINT('',(7.,-9.25,1.));
#14037=CARTESIAN_POINT('Origin',(-7.,-9.25,1.));
#14038=CARTESIAN_POINT('',(-7.,-9.25,1.));
#14039=CARTESIAN_POINT('',(-7.,-9.25,1.));
#14040=CARTESIAN_POINT('',(-7.,-9.25,6.67));
#14041=CARTESIAN_POINT('',(-7.,-9.25,6.67));
#14042=CARTESIAN_POINT('',(-7.,-9.25,1.));
#14043=CARTESIAN_POINT('Origin',(-7.,-4.75,1.));
#14044=CARTESIAN_POINT('',(-7.,-4.75,1.));
#14045=CARTESIAN_POINT('',(-7.,-4.75,6.67));
#14046=CARTESIAN_POINT('Origin',(0.,-7.,6.67));
#14047=CARTESIAN_POINT('Origin',(0.,-7.,1.));
#17207=UNCERTAINTY_MEASURE_WITH_UNIT(LENGTH_MEASURE(0.001),#17323,
'DISTANCE_ACCURACY_VALUE',
'Maximum model space distance between geometric entities at asserted c
onnectivities');
#17261=UNCERTAINTY_MEASURE_WITH_UNIT(LENGTH_MEASURE(0.001),#17323,
'DISTANCE_ACCURACY_VALUE',
'Maximum model space distance between geometric entities at asserted c
onnectivities');
#17268=(
GEOMETRIC_REPRESENTATION_CONTEXT(3)
GLOBAL_UNCERTAINTY_ASSIGNED_CONTEXT((#17207))
GLOBAL_UNIT_ASSIGNED_CONTEXT((#17323,#17325,#17326))
REPRESENTATION_CONTEXT('','3D')
);
#17322=(
GEOMETRIC_REPRESENTATION_CONTEXT(3)
GLOBAL_UNCERTAINTY_ASSIGNED_CONTEXT((#17261))
GLOBAL_UNIT_ASSIGNED_CONTEXT((#17323,#17325,#17326))
REPRESENTATION_CONTEXT('','3D')
);
#17323=(
LENGTH_UNIT()
NAMED_UNIT(*)
SI_UNIT(.CENTI.,.METRE.)
);
#17325=(
NAMED_UNIT(*)
PLANE_ANGLE_UNIT()
SI_UNIT($,.RADIAN.)
);
#17326=(
NAMED_UNIT(*)
SI_UNIT($,.STERADIAN.)
SOLID_ANGLE_UNIT()
);
#17333=SHAPE_DEFINITION_REPRESENTATION(#17393,#17564);
#17393=PRODUCT_DEFINITION_SHAPE('',$,#17625);
#17564=SHAPE_REPRESENTATION('',(#9791),#17268);
#17618=PRODUCT_DEFINITION_CONTEXT('part definition',#17800,'design');
#17625=PRODUCT_DEFINITION('Bearing pedestal (1)','Bearing pedestal (1)',#17685,
#17618);
#17685=PRODUCT_DEFINITION_FORMATION('',$,#17808);
#17800=APPLICATION_CONTEXT(
'Core Data for Automotive Mechanical Design Process');
#17801=PRODUCT_CONTEXT('part definition',#17800,'mechanical');
#17808=PRODUCT('Bearing pedestal (1)','Bearing pedestal (1)',
'Bearing pedestal (1)',(#17801));
#17925=COLOUR_RGB('Grey',0.48,0.52,0.57);
#17926=FILL_AREA_STYLE_COLOUR('',#17925);
#17927=FILL_AREA_STYLE('',(#17926));
#17928=SURFACE_STYLE_FILL_AREA(#17927);
#17929=SURFACE_SIDE_STYLE('',(#17928));
#17930=SURFACE_STYLE_USAGE(.BOTH.,#17929);
#17931=PRESENTATION_STYLE_ASSIGNMENT((#17930));
ENDSEC;
END-ISO-10303-21;
